ISO-10303-21;
HEADER;
/* Generated by software containing ST-Developer
 * from STEP Tools, Inc. (www.steptools.com) 
 */

FILE_DESCRIPTION(
/* description */ ('Independent keyed three-contact power inlet for the IEC-connector des
ign category. Longer ground blade, retained contacts, wire termination
 holes and sealed bolted panel interface. Nominal custom interface; IE
C dimensional compatibility and electrical ratings are not assigned.'),

/* implementation_level */ '2;1');

FILE_NAME(
/* name */ 'Flat washer M6.step',
/* time_stamp */ '2026-11-08T19:55:04-08:00',
/* author */ (''),
/* organization */ (''),
/* preprocessor_version */ 'ST-DEVELOPER v20.2',
/* originating_system */ 'Autodesk Translation Framework v15.17.0.0',
/* authorisation */ '');

FILE_SCHEMA (('AUTOMOTIVE_DESIGN { 1 0 10303 214 3 1 1 }'));
ENDSEC;

DATA;
#10=MECHANICAL_DESIGN_GEOMETRIC_PRESENTATION_REPRESENTATION('',(#117),#21880);
#97=SHAPE_REPRESENTATION_RELATIONSHIP('SRR','None',#21933,#107);
#107=ADVANCED_BREP_SHAPE_REPRESENTATION('',(#127),#21878);
#117=STYLED_ITEM('',(#21988),#127);
#127=MANIFOLD_SOLID_BREP('Body1',#6389);
#193=FACE_BOUND('',#1040,.T.);
#194=FACE_BOUND('',#1042,.T.);
#303=PLANE('',#6923);
#304=PLANE('',#6924);
#643=FACE_OUTER_BOUND('',#1037,.T.);
#644=FACE_OUTER_BOUND('',#1038,.T.);
#645=FACE_OUTER_BOUND('',#1039,.T.);
#646=FACE_OUTER_BOUND('',#1041,.T.);
#1037=EDGE_LOOP('',(#5699,#5700,#5701,#5702));
#1038=EDGE_LOOP('',(#5703,#5704,#5705,#5706));
#1039=EDGE_LOOP('',(#5707));
#1040=EDGE_LOOP('',(#5708));
#1041=EDGE_LOOP('',(#5709));
#1042=EDGE_LOOP('',(#5710));
#1154=CIRCLE('',#6918,3.5);
#1155=CIRCLE('',#6919,3.5);
#1156=CIRCLE('',#6921,7.);
#1157=CIRCLE('',#6922,7.);
#1955=LINE('',#20733,#2411);
#1956=LINE('',#20739,#2412);
#2411=VECTOR('',#8227,3.5);
#2412=VECTOR('',#8234,7.);
#3003=VERTEX_POINT('',#20730);
#3004=VERTEX_POINT('',#20732);
#3005=VERTEX_POINT('',#20736);
#3006=VERTEX_POINT('',#20738);
#3909=EDGE_CURVE('',#3003,#3003,#1154,.T.);
#3910=EDGE_CURVE('',#3003,#3004,#1955,.T.);
#3911=EDGE_CURVE('',#3004,#3004,#1155,.T.);
#3912=EDGE_CURVE('',#3005,#3005,#1156,.T.);
#3913=EDGE_CURVE('',#3005,#3006,#1956,.T.);
#3914=EDGE_CURVE('',#3006,#3006,#1157,.T.);
#5699=ORIENTED_EDGE('',*,*,#3909,.F.);
#5700=ORIENTED_EDGE('',*,*,#3910,.T.);
#5701=ORIENTED_EDGE('',*,*,#3911,.T.);
#5702=ORIENTED_EDGE('',*,*,#3910,.F.);
#5703=ORIENTED_EDGE('',*,*,#3912,.F.);
#5704=ORIENTED_EDGE('',*,*,#3913,.T.);
#5705=ORIENTED_EDGE('',*,*,#3914,.T.);
#5706=ORIENTED_EDGE('',*,*,#3913,.F.);
#5707=ORIENTED_EDGE('',*,*,#3912,.T.);
#5708=ORIENTED_EDGE('',*,*,#3909,.T.);
#5709=ORIENTED_EDGE('',*,*,#3914,.F.);
#5710=ORIENTED_EDGE('',*,*,#3911,.F.);
#6021=CYLINDRICAL_SURFACE('',#6917,3.5);
#6022=CYLINDRICAL_SURFACE('',#6920,7.);
#6355=ADVANCED_FACE('',(#643),#6021,.F.);
#6356=ADVANCED_FACE('',(#644),#6022,.T.);
#6357=ADVANCED_FACE('',(#645,#193),#303,.T.);
#6358=ADVANCED_FACE('',(#646,#194),#304,.F.);
#6389=CLOSED_SHELL('',(#6355,#6356,#6357,#6358));
#6916=AXIS2_PLACEMENT_3D('',#20728,#8221,#8222);
#6917=AXIS2_PLACEMENT_3D('',#20729,#8223,#8224);
#6918=AXIS2_PLACEMENT_3D('',#20731,#8225,#8226);
#6919=AXIS2_PLACEMENT_3D('',#20734,#8228,#8229);
#6920=AXIS2_PLACEMENT_3D('',#20735,#8230,#8231);
#6921=AXIS2_PLACEMENT_3D('',#20737,#8232,#8233);
#6922=AXIS2_PLACEMENT_3D('',#20740,#8235,#8236);
#6923=AXIS2_PLACEMENT_3D('',#20741,#8237,#8238);
#6924=AXIS2_PLACEMENT_3D('',#20742,#8239,#8240);
#8221=DIRECTION('axis',(0.,0.,1.));
#8222=DIRECTION('refdir',(1.,0.,0.));
#8223=DIRECTION('center_axis',(0.,0.,1.));
#8224=DIRECTION('ref_axis',(1.,0.,0.));
#8225=DIRECTION('center_axis',(0.,0.,-1.));
#8226=DIRECTION('ref_axis',(1.,0.,0.));
#8227=DIRECTION('',(0.,0.,-1.));
#8228=DIRECTION('center_axis',(0.,0.,-1.));
#8229=DIRECTION('ref_axis',(1.,0.,0.));
#8230=DIRECTION('center_axis',(0.,0.,1.));
#8231=DIRECTION('ref_axis',(1.,0.,0.));
#8232=DIRECTION('center_axis',(0.,0.,1.));
#8233=DIRECTION('ref_axis',(1.,0.,0.));
#8234=DIRECTION('',(0.,0.,-1.));
#8235=DIRECTION('center_axis',(0.,0.,1.));
#8236=DIRECTION('ref_axis',(1.,0.,0.));
#8237=DIRECTION('center_axis',(0.,0.,1.));
#8238=DIRECTION('ref_axis',(1.,0.,0.));
#8239=DIRECTION('center_axis',(0.,0.,1.));
#8240=DIRECTION('ref_axis',(1.,0.,0.));
#20728=CARTESIAN_POINT('',(0.,0.,0.));
#20729=CARTESIAN_POINT('Origin',(0.,0.,0.));
#20730=CARTESIAN_POINT('',(-3.5,-4.28626379701574E-16,1.));
#20731=CARTESIAN_POINT('Origin',(0.,0.,1.));
#20732=CARTESIAN_POINT('',(-3.5,-4.28626379701574E-16,0.));
#20733=CARTESIAN_POINT('',(-3.5,-4.28626379701574E-16,0.));
#20734=CARTESIAN_POINT('Origin',(0.,0.,0.));
#20735=CARTESIAN_POINT('Origin',(0.,0.,0.));
#20736=CARTESIAN_POINT('',(-7.,-8.57252759403147E-16,1.));
#20737=CARTESIAN_POINT('Origin',(0.,0.,1.));
#20738=CARTESIAN_POINT('',(-7.,-8.57252759403147E-16,0.));
#20739=CARTESIAN_POINT('',(-7.,-8.57252759403147E-16,0.));
#20740=CARTESIAN_POINT('Origin',(0.,0.,0.));
#20741=CARTESIAN_POINT('Origin',(0.,0.,1.));
#20742=CARTESIAN_POINT('Origin',(0.,0.,0.));
#21866=UNCERTAINTY_MEASURE_WITH_UNIT(LENGTH_MEASURE(0.01),#21881,
'DISTANCE_ACCURACY_VALUE',
'Maximum model space distance between geometric entities at asserted c
onnectivities');
#21868=UNCERTAINTY_MEASURE_WITH_UNIT(LENGTH_MEASURE(0.01),#21881,
'DISTANCE_ACCURACY_VALUE',
'Maximum model space distance between geometric entities at asserted c
onnectivities');
#21878=(
GEOMETRIC_REPRESENTATION_CONTEXT(3)
GLOBAL_UNCERTAINTY_ASSIGNED_CONTEXT((#21866))
GLOBAL_UNIT_ASSIGNED_CONTEXT((#21881,#21883,#21884))
REPRESENTATION_CONTEXT('','3D')
);
#21880=(
GEOMETRIC_REPRESENTATION_CONTEXT(3)
GLOBAL_UNCERTAINTY_ASSIGNED_CONTEXT((#21868))
GLOBAL_UNIT_ASSIGNED_CONTEXT((#21881,#21883,#21884))
REPRESENTATION_CONTEXT('','3D')
);
#21881=(
LENGTH_UNIT()
NAMED_UNIT(*)
SI_UNIT(.MILLI.,.METRE.)
);
#21883=(
NAMED_UNIT(*)
PLANE_ANGLE_UNIT()
SI_UNIT($,.RADIAN.)
);
#21884=(
NAMED_UNIT(*)
SI_UNIT($,.STERADIAN.)
SOLID_ANGLE_UNIT()
);
#21894=SHAPE_DEFINITION_REPRESENTATION(#21905,#21933);
#21905=PRODUCT_DEFINITION_SHAPE('',$,#21945);
#21933=SHAPE_REPRESENTATION('',(#6916),#21878);
#21935=PRODUCT_DEFINITION_CONTEXT('part definition',#21970,'design');
#21945=PRODUCT_DEFINITION('Flat washer M6','Flat washer M6',#21956,#21935);
#21956=PRODUCT_DEFINITION_FORMATION('',$,#21981);
#21970=APPLICATION_CONTEXT(
'Core Data for Automotive Mechanical Design Process');
#21971=PRODUCT_CONTEXT('part definition',#21970,'mechanical');
#21981=PRODUCT('Flat washer M6','Flat washer M6',$,(#21971));
#21988=PRESENTATION_STYLE_ASSIGNMENT((#21994));
#21994=SURFACE_STYLE_USAGE(.BOTH.,#22000);
#22000=SURFACE_SIDE_STYLE('',(#22006));
#22006=SURFACE_STYLE_FILL_AREA(#22012);
#22012=FILL_AREA_STYLE('Light gray',(#22018));
#22018=FILL_AREA_STYLE_COLOUR('Light gray',#22024);
#22024=COLOUR_RGB('Light gray',0.725490196078431,0.752941176470588,0.792156862745098);
ENDSEC;
END-ISO-10303-21;
